ISO-10303-21;
HEADER;
/* Generated by software containing ST-Developer
 * from STEP Tools, Inc. (www.steptools.com) 
 */

FILE_DESCRIPTION(
/* description */ ('Fatigue rig crank-slider'),
/* implementation_level */ '2;1');

FILE_NAME(
/* name */ 'Bearing bolt reducer (1).step',
/* time_stamp */ '2026-10-28T03:24:50-07:00',
/* author */ (''),
/* organization */ (''),
/* preprocessor_version */ 'ST-DEVELOPER v20.2',
/* originating_system */ 'Autodesk Translation Framework v15.17.0.0',
/* authorisation */ '');

FILE_SCHEMA (('AUTOMOTIVE_DESIGN { 1 0 10303 214 3 1 1 }'));
ENDSEC;

DATA;
#10=MECHANICAL_DESIGN_GEOMETRIC_PRESENTATION_REPRESENTATION('',(#590),#16911);
#490=SHAPE_REPRESENTATION_RELATIONSHIP('SRR','None',#17129,#540);
#540=ADVANCED_BREP_SHAPE_REPRESENTATION('',(#649),#16858);
#590=STYLED_ITEM('',(#17494),#649);
#649=MANIFOLD_SOLID_BREP('Body1',#8881);
#740=FACE_BOUND('',#1827,.T.);
#741=FACE_BOUND('',#1829,.T.);
#917=PLANE('',#9597);
#918=PLANE('',#9598);
#1261=FACE_OUTER_BOUND('',#1824,.T.);
#1262=FACE_OUTER_BOUND('',#1825,.T.);
#1263=FACE_OUTER_BOUND('',#1826,.T.);
#1264=FACE_OUTER_BOUND('',#1828,.T.);
#1824=EDGE_LOOP('',(#6188,#6189,#6190,#6191));
#1825=EDGE_LOOP('',(#6192,#6193,#6194,#6195));
#1826=EDGE_LOOP('',(#6196));
#1827=EDGE_LOOP('',(#6197));
#1828=EDGE_LOOP('',(#6198));
#1829=EDGE_LOOP('',(#6199));
#2508=LINE('',#13572,#3154);
#2509=LINE('',#13578,#3155);
#3154=VECTOR('',#10814,0.425);
#3155=VECTOR('',#10821,0.645);
#3800=CIRCLE('',#9592,0.425);
#3801=CIRCLE('',#9593,0.425);
#3802=CIRCLE('',#9595,0.645);
#3803=CIRCLE('',#9596,0.645);
#4216=VERTEX_POINT('',#13569);
#4217=VERTEX_POINT('',#13571);
#4218=VERTEX_POINT('',#13575);
#4219=VERTEX_POINT('',#13577);
#4992=EDGE_CURVE('',#4216,#4216,#3800,.T.);
#4993=EDGE_CURVE('',#4216,#4217,#2508,.T.);
#4994=EDGE_CURVE('',#4217,#4217,#3801,.T.);
#4995=EDGE_CURVE('',#4218,#4218,#3802,.T.);
#4996=EDGE_CURVE('',#4218,#4219,#2509,.T.);
#4997=EDGE_CURVE('',#4219,#4219,#3803,.T.);
#6188=ORIENTED_EDGE('',*,*,#4992,.F.);
#6189=ORIENTED_EDGE('',*,*,#4993,.T.);
#6190=ORIENTED_EDGE('',*,*,#4994,.T.);
#6191=ORIENTED_EDGE('',*,*,#4993,.F.);
#6192=ORIENTED_EDGE('',*,*,#4995,.F.);
#6193=ORIENTED_EDGE('',*,*,#4996,.T.);
#6194=ORIENTED_EDGE('',*,*,#4997,.T.);
#6195=ORIENTED_EDGE('',*,*,#4996,.F.);
#6196=ORIENTED_EDGE('',*,*,#4995,.T.);
#6197=ORIENTED_EDGE('',*,*,#4992,.T.);
#6198=ORIENTED_EDGE('',*,*,#4997,.F.);
#6199=ORIENTED_EDGE('',*,*,#4994,.F.);
#8220=CYLINDRICAL_SURFACE('',#9591,0.425);
#8221=CYLINDRICAL_SURFACE('',#9594,0.645);
#8399=ADVANCED_FACE('',(#1261),#8220,.F.);
#8400=ADVANCED_FACE('',(#1262),#8221,.T.);
#8401=ADVANCED_FACE('',(#1263,#740),#917,.T.);
#8402=ADVANCED_FACE('',(#1264,#741),#918,.F.);
#8881=CLOSED_SHELL('',(#8399,#8400,#8401,#8402));
#9590=AXIS2_PLACEMENT_3D('',#13567,#10808,#10809);
#9591=AXIS2_PLACEMENT_3D('',#13568,#10810,#10811);
#9592=AXIS2_PLACEMENT_3D('',#13570,#10812,#10813);
#9593=AXIS2_PLACEMENT_3D('',#13573,#10815,#10816);
#9594=AXIS2_PLACEMENT_3D('',#13574,#10817,#10818);
#9595=AXIS2_PLACEMENT_3D('',#13576,#10819,#10820);
#9596=AXIS2_PLACEMENT_3D('',#13579,#10822,#10823);
#9597=AXIS2_PLACEMENT_3D('',#13580,#10824,#10825);
#9598=AXIS2_PLACEMENT_3D('',#13581,#10826,#10827);
#10808=DIRECTION('axis',(0.,0.,1.));
#10809=DIRECTION('refdir',(1.,0.,0.));
#10810=DIRECTION('center_axis',(0.,0.,1.));
#10811=DIRECTION('ref_axis',(1.,0.,0.));
#10812=DIRECTION('center_axis',(0.,0.,-1.));
#10813=DIRECTION('ref_axis',(1.,0.,0.));
#10814=DIRECTION('',(0.,0.,-1.));
#10815=DIRECTION('center_axis',(0.,0.,-1.));
#10816=DIRECTION('ref_axis',(1.,0.,0.));
#10817=DIRECTION('center_axis',(0.,0.,1.));
#10818=DIRECTION('ref_axis',(1.,0.,0.));
#10819=DIRECTION('center_axis',(0.,0.,1.));
#10820=DIRECTION('ref_axis',(1.,0.,0.));
#10821=DIRECTION('',(0.,0.,-1.));
#10822=DIRECTION('center_axis',(0.,0.,1.));
#10823=DIRECTION('ref_axis',(1.,0.,0.));
#10824=DIRECTION('center_axis',(0.,0.,1.));
#10825=DIRECTION('ref_axis',(1.,0.,0.));
#10826=DIRECTION('center_axis',(0.,0.,1.));
#10827=DIRECTION('ref_axis',(1.,0.,0.));
#13567=CARTESIAN_POINT('',(0.,0.,0.));
#13568=CARTESIAN_POINT('Origin',(4.75,-15.,8.67));
#13569=CARTESIAN_POINT('',(4.325,-15.,9.87));
#13570=CARTESIAN_POINT('Origin',(4.75,-15.,9.87));
#13571=CARTESIAN_POINT('',(4.325,-15.,8.67));
#13572=CARTESIAN_POINT('',(4.325,-15.,8.67));
#13573=CARTESIAN_POINT('Origin',(4.75,-15.,8.67));
#13574=CARTESIAN_POINT('Origin',(4.75,-15.,8.67));
#13575=CARTESIAN_POINT('',(4.105,-15.,9.87));
#13576=CARTESIAN_POINT('Origin',(4.75,-15.,9.87));
#13577=CARTESIAN_POINT('',(4.105,-15.,8.67));
#13578=CARTESIAN_POINT('',(4.105,-15.,8.67));
#13579=CARTESIAN_POINT('Origin',(4.75,-15.,8.67));
#13580=CARTESIAN_POINT('Origin',(4.75,-15.,9.87));
#13581=CARTESIAN_POINT('Origin',(4.75,-15.,8.67));
#16799=UNCERTAINTY_MEASURE_WITH_UNIT(LENGTH_MEASURE(0.001),#16912,
'DISTANCE_ACCURACY_VALUE',
'Maximum model space distance between geometric entities at asserted c
onnectivities');
#16852=UNCERTAINTY_MEASURE_WITH_UNIT(LENGTH_MEASURE(0.001),#16912,
'DISTANCE_ACCURACY_VALUE',
'Maximum model space distance between geometric entities at asserted c
onnectivities');
#16858=(
GEOMETRIC_REPRESENTATION_CONTEXT(3)
GLOBAL_UNCERTAINTY_ASSIGNED_CONTEXT((#16799))
GLOBAL_UNIT_ASSIGNED_CONTEXT((#16912,#16914,#16915))
REPRESENTATION_CONTEXT('','3D')
);
#16911=(
GEOMETRIC_REPRESENTATION_CONTEXT(3)
GLOBAL_UNCERTAINTY_ASSIGNED_CONTEXT((#16852))
GLOBAL_UNIT_ASSIGNED_CONTEXT((#16912,#16914,#16915))
REPRESENTATION_CONTEXT('','3D')
);
#16912=(
LENGTH_UNIT()
NAMED_UNIT(*)
SI_UNIT(.CENTI.,.METRE.)
);
#16914=(
NAMED_UNIT(*)
PLANE_ANGLE_UNIT()
SI_UNIT($,.RADIAN.)
);
#16915=(
NAMED_UNIT(*)
SI_UNIT($,.STERADIAN.)
SOLID_ANGLE_UNIT()
);
#16921=SHAPE_DEFINITION_REPRESENTATION(#16979,#17129);
#16979=PRODUCT_DEFINITION_SHAPE('',$,#17188);
#17129=SHAPE_REPRESENTATION('',(#9590),#16858);
#17182=PRODUCT_DEFINITION_CONTEXT('part definition',#17358,'design');
#17188=PRODUCT_DEFINITION('Bearing bolt reducer (1)',
'Bearing bolt reducer (1)',#17246,#17182);
#17246=PRODUCT_DEFINITION_FORMATION('',$,#17365);
#17358=APPLICATION_CONTEXT(
'Core Data for Automotive Mechanical Design Process');
#17359=PRODUCT_CONTEXT('part definition',#17358,'mechanical');
#17365=PRODUCT('Bearing bolt reducer (1)','Bearing bolt reducer (1)',
'Bearing bolt reducer (1)',(#17359));
#17488=COLOUR_RGB('Black',0.12,0.14,0.17);
#17489=FILL_AREA_STYLE_COLOUR('',#17488);
#17490=FILL_AREA_STYLE('',(#17489));
#17491=SURFACE_STYLE_FILL_AREA(#17490);
#17492=SURFACE_SIDE_STYLE('',(#17491));
#17493=SURFACE_STYLE_USAGE(.BOTH.,#17492);
#17494=PRESENTATION_STYLE_ASSIGNMENT((#17493));
ENDSEC;
END-ISO-10303-21;
